ISO-10303-21;
HEADER;
/* Generated by software containing ST-Developer
 * from STEP Tools, Inc. (www.steptools.com) 
 */
/* OPTION: using custom renumber hook */

FILE_DESCRIPTION(
/* description */ ('STEP AP242 Edition 2', 'CAx-IF Rec.Pracs.---Representation and Presentation of Product Manufa
cturing Information (PMI)---4.0---2014-10-13', 'CAx-IF Rec.Pracs.---3D Tessellated Geometry---0.4---2014-09-14', '2;1', 'CAx-IF Rec.Pracs.---User Defined Attributes---1.5---2016-08-15'),
/* implementation_level */ '2;1');

FILE_NAME(
/* name */ 'Part 1.step',
/* time_stamp */ '2026-10-07T00:00:55Z',
/* author */ (''),
/* organization */ (''),
/* preprocessor_version */ 'ST-DEVELOPER v20',
/* originating_system */ 'ONSHAPE BY PTC INC, 1.221',
/* authorisation */ '  ');

FILE_SCHEMA (('AP242_MANAGED_MODEL_BASED_3D_ENGINEERING_MIM_LF { 1 0 10303 442 3 1 4 }'));
ENDSEC;

DATA;
#118=SHAPE_REPRESENTATION_RELATIONSHIP('','',#4474,#129);
#129=ADVANCED_BREP_SHAPE_REPRESENTATION('',(#4450),#8537);
#205=CYLINDRICAL_SURFACE('',#4520,0.041);
#206=CYLINDRICAL_SURFACE('',#4521,0.039);
#318=CIRCLE('',#4515,0.041);
#319=CIRCLE('',#4516,0.039);
#320=CIRCLE('',#4518,0.041);
#321=CIRCLE('',#4519,0.039);
#767=ORIENTED_EDGE('',*,*,#1903,.T.);
#768=ORIENTED_EDGE('',*,*,#1904,.F.);
#769=ORIENTED_EDGE('',*,*,#1905,.F.);
#770=ORIENTED_EDGE('',*,*,#1906,.T.);
#771=ORIENTED_EDGE('',*,*,#1903,.F.);
#772=ORIENTED_EDGE('',*,*,#1905,.T.);
#773=ORIENTED_EDGE('',*,*,#1904,.T.);
#774=ORIENTED_EDGE('',*,*,#1906,.F.);
#1903=EDGE_CURVE('',#2476,#2476,#318,.T.);
#1904=EDGE_CURVE('',#2477,#2477,#319,.T.);
#1905=EDGE_CURVE('',#2478,#2478,#320,.T.);
#1906=EDGE_CURVE('',#2479,#2479,#321,.T.);
#2476=VERTEX_POINT('',#6516);
#2477=VERTEX_POINT('',#6518);
#2478=VERTEX_POINT('',#6521);
#2479=VERTEX_POINT('',#6523);
#3212=EDGE_LOOP('',(#767));
#3213=EDGE_LOOP('',(#768));
#3214=EDGE_LOOP('',(#769));
#3215=EDGE_LOOP('',(#770));
#3216=EDGE_LOOP('',(#771));
#3217=EDGE_LOOP('',(#772));
#3218=EDGE_LOOP('',(#773));
#3219=EDGE_LOOP('',(#774));
#3589=FACE_BOUND('',#3212,.T.);
#3590=FACE_BOUND('',#3213,.T.);
#3591=FACE_BOUND('',#3214,.T.);
#3592=FACE_BOUND('',#3215,.T.);
#3593=FACE_BOUND('',#3216,.T.);
#3594=FACE_BOUND('',#3217,.T.);
#3595=FACE_BOUND('',#3218,.T.);
#3596=FACE_BOUND('',#3219,.T.);
#3953=PLANE('',#4514);
#3954=PLANE('',#4517);
#4054=ADVANCED_FACE('',(#3589,#3590),#3953,.T.);
#4055=ADVANCED_FACE('',(#3591,#3592),#3954,.F.);
#4056=ADVANCED_FACE('',(#3593,#3594),#205,.T.);
#4057=ADVANCED_FACE('',(#3595,#3596),#206,.F.);
#4324=CLOSED_SHELL('',(#4054,#4055,#4056,#4057));
#4335=STYLED_ITEM('',(#4346),#4450);
#4346=PRESENTATION_STYLE_ASSIGNMENT((#4362));
#4362=SURFACE_STYLE_USAGE(.BOTH.,#4378);
#4378=SURFACE_SIDE_STYLE('',(#4394));
#4394=SURFACE_STYLE_FILL_AREA(#4410);
#4410=FILL_AREA_STYLE('',(#4426));
#4426=FILL_AREA_STYLE_COLOUR('',#4442);
#4442=COLOUR_RGB('', 0.31764706, 0.68627451, 0.89019608);
#4450=MANIFOLD_SOLID_BREP('Part 1',#4324);
#4462=SHAPE_DEFINITION_REPRESENTATION(#8565,#4474);
#4474=SHAPE_REPRESENTATION('Part 1',(#4484),#8537);
#4484=AXIS2_PLACEMENT_3D('',#6402,#5064,#5065);
#4514=AXIS2_PLACEMENT_3D('',#6514,#5136,#5137);
#4515=AXIS2_PLACEMENT_3D('',#6515,#5138,#5139);
#4516=AXIS2_PLACEMENT_3D('',#6517,#5140,#5141);
#4517=AXIS2_PLACEMENT_3D('',#6519,#5142,#5143);
#4518=AXIS2_PLACEMENT_3D('',#6520,#5144,#5145);
#4519=AXIS2_PLACEMENT_3D('',#6522,#5146,#5147);
#4520=AXIS2_PLACEMENT_3D('',#6524,#5148,#5149);
#4521=AXIS2_PLACEMENT_3D('',#6525,#5150,#5151);
#5064=DIRECTION('',(0.,0.,1.));
#5065=DIRECTION('',(1.,0.,0.));
#5136=DIRECTION('',(0.,1.,0.));
#5137=DIRECTION('',(0.,0.,1.));
#5138=DIRECTION('',(0.,1.,0.));
#5139=DIRECTION('',(1.,0.,0.));
#5140=DIRECTION('',(0.,1.,0.));
#5141=DIRECTION('',(0.,0.,1.));
#5142=DIRECTION('',(0.,1.,0.));
#5143=DIRECTION('',(0.,0.,1.));
#5144=DIRECTION('',(0.,1.,0.));
#5145=DIRECTION('',(1.,0.,0.));
#5146=DIRECTION('',(0.,1.,0.));
#5147=DIRECTION('',(0.,0.,1.));
#5148=DIRECTION('',(0.,-1.,0.));
#5149=DIRECTION('',(0.,0.,-1.));
#5150=DIRECTION('',(0.,-1.,0.));
#5151=DIRECTION('',(0.,0.,-1.));
#6402=CARTESIAN_POINT('',(0.,0.,0.));
#6514=CARTESIAN_POINT('',(0.,0.09,0.));
#6515=CARTESIAN_POINT('',(0.,0.09,0.));
#6516=CARTESIAN_POINT('',(0.041,0.09,0.));
#6517=CARTESIAN_POINT('',(0.,0.09,0.));
#6518=CARTESIAN_POINT('',(0.,0.09,0.039));
#6519=CARTESIAN_POINT('',(0.,0.,0.));
#6520=CARTESIAN_POINT('',(0.,0.,0.));
#6521=CARTESIAN_POINT('',(0.041,0.,0.));
#6522=CARTESIAN_POINT('',(0.,0.,0.));
#6523=CARTESIAN_POINT('',(0.,0.,0.039));
#6524=CARTESIAN_POINT('',(0.,0.09,0.));
#6525=CARTESIAN_POINT('',(0.,0.09,0.));
#8534=MECHANICAL_DESIGN_GEOMETRIC_PRESENTATION_REPRESENTATION('',(#4335),#8535);
#8535=(
GEOMETRIC_REPRESENTATION_CONTEXT(3)
GLOBAL_UNCERTAINTY_ASSIGNED_CONTEXT((#8547))
GLOBAL_UNIT_ASSIGNED_CONTEXT((#8561,#8560,#8559))
REPRESENTATION_CONTEXT('MAS-680','TOP_LEVEL_ASSEMBLY_PART')
);
#8537=(
GEOMETRIC_REPRESENTATION_CONTEXT(3)
GLOBAL_UNCERTAINTY_ASSIGNED_CONTEXT((#8549))
GLOBAL_UNIT_ASSIGNED_CONTEXT((#8561,#8560,#8559))
REPRESENTATION_CONTEXT('Part 1','COMPONENT_PART')
);
#8547=UNCERTAINTY_MEASURE_WITH_UNIT(LENGTH_MEASURE(1.E-8),#8561,
'DISTANCE_ACCURACY_VALUE','Maximum Tolerance applied to model');
#8549=UNCERTAINTY_MEASURE_WITH_UNIT(LENGTH_MEASURE(1.E-8),#8561,
'DISTANCE_ACCURACY_VALUE','Maximum Tolerance applied to model');
#8559=(
NAMED_UNIT(*)
SI_UNIT($,.STERADIAN.)
SOLID_ANGLE_UNIT()
);
#8560=(
NAMED_UNIT(*)
PLANE_ANGLE_UNIT()
SI_UNIT($,.RADIAN.)
);
#8561=(
LENGTH_UNIT()
NAMED_UNIT(*)
SI_UNIT($,.METRE.)
);
#8565=PRODUCT_DEFINITION_SHAPE('','',#8591);
#8591=PRODUCT_DEFINITION('','',#8615,#8603);
#8603=PRODUCT_DEFINITION_CONTEXT('',#8674,'design');
#8615=PRODUCT_DEFINITION_FORMATION_WITH_SPECIFIED_SOURCE('','',#8639,
 .NOT_KNOWN.);
#8639=PRODUCT('Part 1','Part 1','Part 1',(#8663));
#8663=PRODUCT_CONTEXT('',#8674,'mechanical');
#8674=APPLICATION_CONTEXT('managed model based 3d engineering');
ENDSEC;
END-ISO-10303-21;
